ISO-10303-21;
HEADER;
/* Generated by software containing ST-Developer
 * from STEP Tools, Inc. (www.steptools.com) 
 */

FILE_DESCRIPTION(
/* description */ ('Hand-operated arbor press'),
/* implementation_level */ '2;1');

FILE_NAME(
/* name */ 'M4x10 Cap Screw.step',
/* time_stamp */ '2026-10-28T03:25:25-07:00',
/* author */ (''),
/* organization */ (''),
/* preprocessor_version */ 'ST-DEVELOPER v20.2',
/* originating_system */ 'Autodesk Translation Framework v15.17.0.0',
/* authorisation */ '');

FILE_SCHEMA (('AUTOMOTIVE_DESIGN { 1 0 10303 214 3 1 1 }'));
ENDSEC;

DATA;
#10=MECHANICAL_DESIGN_GEOMETRIC_PRESENTATION_REPRESENTATION('',(#614),#32751);
#474=ORIENTED_CLOSED_SHELL('',*,#12512,.F.);
#485=CONICAL_SURFACE('',#13555,0.325,0.785398163397448);
#486=CONICAL_SURFACE('',#13559,0.335,0.785398163397448);
#487=CONICAL_SURFACE('',#13563,0.21,0.463647609000806);
#499=BREP_WITH_VOIDS('Body1',#12513,(#474));
#523=SHAPE_REPRESENTATION_RELATIONSHIP('SRR','None',#32953,#565);
#565=ADVANCED_BREP_SHAPE_REPRESENTATION('',(#499),#32727);
#614=STYLED_ITEM('',(#33249),#499);
#811=FACE_BOUND('',#2386,.T.);
#993=PLANE('',#13543);
#994=PLANE('',#13544);
#995=PLANE('',#13545);
#996=PLANE('',#13546);
#997=PLANE('',#13547);
#998=PLANE('',#13548);
#999=PLANE('',#13549);
#1000=PLANE('',#13550);
#1001=PLANE('',#13551);
#1002=PLANE('',#13553);
#1003=PLANE('',#13561);
#1560=FACE_OUTER_BOUND('',#2372,.T.);
#1561=FACE_OUTER_BOUND('',#2373,.T.);
#1562=FACE_OUTER_BOUND('',#2374,.T.);
#1563=FACE_OUTER_BOUND('',#2375,.T.);
#1564=FACE_OUTER_BOUND('',#2376,.T.);
#1565=FACE_OUTER_BOUND('',#2377,.T.);
#1566=FACE_OUTER_BOUND('',#2378,.T.);
#1567=FACE_OUTER_BOUND('',#2379,.T.);
#1568=FACE_OUTER_BOUND('',#2380,.T.);
#1569=FACE_OUTER_BOUND('',#2381,.T.);
#1570=FACE_OUTER_BOUND('',#2382,.T.);
#1571=FACE_OUTER_BOUND('',#2383,.T.);
#1572=FACE_OUTER_BOUND('',#2384,.T.);
#1573=FACE_OUTER_BOUND('',#2385,.T.);
#1574=FACE_OUTER_BOUND('',#2387,.T.);
#1575=FACE_OUTER_BOUND('',#2388,.T.);
#2372=EDGE_LOOP('',(#9540,#9541,#9542,#9543));
#2373=EDGE_LOOP('',(#9544,#9545,#9546,#9547));
#2374=EDGE_LOOP('',(#9548,#9549,#9550,#9551));
#2375=EDGE_LOOP('',(#9552,#9553,#9554,#9555));
#2376=EDGE_LOOP('',(#9556,#9557,#9558,#9559));
#2377=EDGE_LOOP('',(#9560,#9561,#9562,#9563));
#2378=EDGE_LOOP('',(#9564,#9565,#9566,#9567,#9568,#9569));
#2379=EDGE_LOOP('',(#9570,#9571,#9572,#9573,#9574,#9575));
#2380=EDGE_LOOP('',(#9576));
#2381=EDGE_LOOP('',(#9577));
#2382=EDGE_LOOP('',(#9578,#9579,#9580,#9581));
#2383=EDGE_LOOP('',(#9582,#9583,#9584,#9585));
#2384=EDGE_LOOP('',(#9586,#9587,#9588,#9589));
#2385=EDGE_LOOP('',(#9590));
#2386=EDGE_LOOP('',(#9591));
#2387=EDGE_LOOP('',(#9592,#9593,#9594,#9595));
#2388=EDGE_LOOP('',(#9596,#9597,#9598,#9599));
#3171=LINE('',#19252,#4342);
#3172=LINE('',#19254,#4343);
#3173=LINE('',#19256,#4344);
#3174=LINE('',#19257,#4345);
#3175=LINE('',#19260,#4346);
#3176=LINE('',#19262,#4347);
#3177=LINE('',#19263,#4348);
#3178=LINE('',#19266,#4349);
#3179=LINE('',#19268,#4350);
#3180=LINE('',#19269,#4351);
#3181=LINE('',#19272,#4352);
#3182=LINE('',#19274,#4353);
#3183=LINE('',#19275,#4354);
#3184=LINE('',#19278,#4355);
#3185=LINE('',#19280,#4356);
#3186=LINE('',#19281,#4357);
#3187=LINE('',#19283,#4358);
#3188=LINE('',#19284,#4359);
#3189=LINE('',#19296,#4360);
#3190=LINE('',#19300,#4361);
#3191=LINE('',#19304,#4362);
#3192=LINE('',#19311,#4363);
#3193=LINE('',#19313,#4364);
#4342=VECTOR('',#15592,1.);
#4343=VECTOR('',#15593,1.);
#4344=VECTOR('',#15594,1.);
#4345=VECTOR('',#15595,1.);
#4346=VECTOR('',#15598,1.);
#4347=VECTOR('',#15599,1.);
#4348=VECTOR('',#15600,1.);
#4349=VECTOR('',#15603,1.);
#4350=VECTOR('',#15604,1.);
#4351=VECTOR('',#15605,1.);
#4352=VECTOR('',#15608,1.);
#4353=VECTOR('',#15609,1.);
#4354=VECTOR('',#15610,1.);
#4355=VECTOR('',#15613,1.);
#4356=VECTOR('',#15614,1.);
#4357=VECTOR('',#15615,1.);
#4358=VECTOR('',#15618,1.);
#4359=VECTOR('',#15619,1.);
#4360=VECTOR('',#15636,0.325);
#4361=VECTOR('',#15641,0.35);
#4362=VECTOR('',#15646,0.335);
#4363=VECTOR('',#15655,0.21);
#4364=VECTOR('',#15658,0.2);
#5413=CIRCLE('',#13552,0.1954);
#5414=CIRCLE('',#13554,0.3);
#5415=CIRCLE('',#13556,0.35);
#5416=CIRCLE('',#13558,0.35);
#5417=CIRCLE('',#13560,0.32);
#5418=CIRCLE('',#13562,0.22);
#5419=CIRCLE('',#13564,0.1954);
#5968=VERTEX_POINT('',#19250);
#5969=VERTEX_POINT('',#19251);
#5970=VERTEX_POINT('',#19253);
#5971=VERTEX_POINT('',#19255);
#5972=VERTEX_POINT('',#19259);
#5973=VERTEX_POINT('',#19261);
#5974=VERTEX_POINT('',#19265);
#5975=VERTEX_POINT('',#19267);
#5976=VERTEX_POINT('',#19271);
#5977=VERTEX_POINT('',#19273);
#5978=VERTEX_POINT('',#19277);
#5979=VERTEX_POINT('',#19279);
#5980=VERTEX_POINT('',#19288);
#5981=VERTEX_POINT('',#19291);
#5982=VERTEX_POINT('',#19294);
#5983=VERTEX_POINT('',#19298);
#5984=VERTEX_POINT('',#19302);
#5985=VERTEX_POINT('',#19306);
#5986=VERTEX_POINT('',#19309);
#7273=EDGE_CURVE('',#5968,#5969,#3171,.T.);
#7274=EDGE_CURVE('',#5969,#5970,#3172,.T.);
#7275=EDGE_CURVE('',#5970,#5971,#3173,.T.);
#7276=EDGE_CURVE('',#5968,#5971,#3174,.T.);
#7277=EDGE_CURVE('',#5969,#5972,#3175,.T.);
#7278=EDGE_CURVE('',#5972,#5973,#3176,.T.);
#7279=EDGE_CURVE('',#5973,#5970,#3177,.T.);
#7280=EDGE_CURVE('',#5972,#5974,#3178,.T.);
#7281=EDGE_CURVE('',#5974,#5975,#3179,.T.);
#7282=EDGE_CURVE('',#5975,#5973,#3180,.T.);
#7283=EDGE_CURVE('',#5974,#5976,#3181,.T.);
#7284=EDGE_CURVE('',#5976,#5977,#3182,.T.);
#7285=EDGE_CURVE('',#5977,#5975,#3183,.T.);
#7286=EDGE_CURVE('',#5976,#5978,#3184,.T.);
#7287=EDGE_CURVE('',#5978,#5979,#3185,.T.);
#7288=EDGE_CURVE('',#5979,#5977,#3186,.T.);
#7289=EDGE_CURVE('',#5978,#5968,#3187,.T.);
#7290=EDGE_CURVE('',#5971,#5979,#3188,.T.);
#7291=EDGE_CURVE('',#5980,#5980,#5413,.T.);
#7292=EDGE_CURVE('',#5981,#5981,#5414,.T.);
#7293=EDGE_CURVE('',#5982,#5982,#5415,.T.);
#7294=EDGE_CURVE('',#5982,#5981,#3189,.T.);
#7295=EDGE_CURVE('',#5983,#5983,#5416,.T.);
#7296=EDGE_CURVE('',#5983,#5982,#3190,.T.);
#7297=EDGE_CURVE('',#5984,#5984,#5417,.T.);
#7298=EDGE_CURVE('',#5984,#5983,#3191,.T.);
#7299=EDGE_CURVE('',#5985,#5985,#5418,.T.);
#7300=EDGE_CURVE('',#5986,#5986,#5419,.F.);
#7301=EDGE_CURVE('',#5986,#5985,#3192,.T.);
#7302=EDGE_CURVE('',#5980,#5986,#3193,.T.);
#9540=ORIENTED_EDGE('',*,*,#7273,.T.);
#9541=ORIENTED_EDGE('',*,*,#7274,.T.);
#9542=ORIENTED_EDGE('',*,*,#7275,.T.);
#9543=ORIENTED_EDGE('',*,*,#7276,.F.);
#9544=ORIENTED_EDGE('',*,*,#7277,.T.);
#9545=ORIENTED_EDGE('',*,*,#7278,.T.);
#9546=ORIENTED_EDGE('',*,*,#7279,.T.);
#9547=ORIENTED_EDGE('',*,*,#7274,.F.);
#9548=ORIENTED_EDGE('',*,*,#7280,.T.);
#9549=ORIENTED_EDGE('',*,*,#7281,.T.);
#9550=ORIENTED_EDGE('',*,*,#7282,.T.);
#9551=ORIENTED_EDGE('',*,*,#7278,.F.);
#9552=ORIENTED_EDGE('',*,*,#7283,.T.);
#9553=ORIENTED_EDGE('',*,*,#7284,.T.);
#9554=ORIENTED_EDGE('',*,*,#7285,.T.);
#9555=ORIENTED_EDGE('',*,*,#7281,.F.);
#9556=ORIENTED_EDGE('',*,*,#7286,.T.);
#9557=ORIENTED_EDGE('',*,*,#7287,.T.);
#9558=ORIENTED_EDGE('',*,*,#7288,.T.);
#9559=ORIENTED_EDGE('',*,*,#7284,.F.);
#9560=ORIENTED_EDGE('',*,*,#7289,.T.);
#9561=ORIENTED_EDGE('',*,*,#7276,.T.);
#9562=ORIENTED_EDGE('',*,*,#7290,.T.);
#9563=ORIENTED_EDGE('',*,*,#7287,.F.);
#9564=ORIENTED_EDGE('',*,*,#7289,.F.);
#9565=ORIENTED_EDGE('',*,*,#7286,.F.);
#9566=ORIENTED_EDGE('',*,*,#7283,.F.);
#9567=ORIENTED_EDGE('',*,*,#7280,.F.);
#9568=ORIENTED_EDGE('',*,*,#7277,.F.);
#9569=ORIENTED_EDGE('',*,*,#7273,.F.);
#9570=ORIENTED_EDGE('',*,*,#7290,.F.);
#9571=ORIENTED_EDGE('',*,*,#7275,.F.);
#9572=ORIENTED_EDGE('',*,*,#7279,.F.);
#9573=ORIENTED_EDGE('',*,*,#7282,.F.);
#9574=ORIENTED_EDGE('',*,*,#7285,.F.);
#9575=ORIENTED_EDGE('',*,*,#7288,.F.);
#9576=ORIENTED_EDGE('',*,*,#7291,.F.);
#9577=ORIENTED_EDGE('',*,*,#7292,.F.);
#9578=ORIENTED_EDGE('',*,*,#7293,.F.);
#9579=ORIENTED_EDGE('',*,*,#7294,.T.);
#9580=ORIENTED_EDGE('',*,*,#7292,.T.);
#9581=ORIENTED_EDGE('',*,*,#7294,.F.);
#9582=ORIENTED_EDGE('',*,*,#7295,.F.);
#9583=ORIENTED_EDGE('',*,*,#7296,.T.);
#9584=ORIENTED_EDGE('',*,*,#7293,.T.);
#9585=ORIENTED_EDGE('',*,*,#7296,.F.);
#9586=ORIENTED_EDGE('',*,*,#7297,.F.);
#9587=ORIENTED_EDGE('',*,*,#7298,.T.);
#9588=ORIENTED_EDGE('',*,*,#7295,.T.);
#9589=ORIENTED_EDGE('',*,*,#7298,.F.);
#9590=ORIENTED_EDGE('',*,*,#7297,.T.);
#9591=ORIENTED_EDGE('',*,*,#7299,.F.);
#9592=ORIENTED_EDGE('',*,*,#7300,.F.);
#9593=ORIENTED_EDGE('',*,*,#7301,.T.);
#9594=ORIENTED_EDGE('',*,*,#7299,.T.);
#9595=ORIENTED_EDGE('',*,*,#7301,.F.);
#9596=ORIENTED_EDGE('',*,*,#7291,.T.);
#9597=ORIENTED_EDGE('',*,*,#7302,.T.);
#9598=ORIENTED_EDGE('',*,*,#7300,.T.);
#9599=ORIENTED_EDGE('',*,*,#7302,.F.);
#11741=CYLINDRICAL_SURFACE('',#13557,0.35);
#11742=CYLINDRICAL_SURFACE('',#13565,0.1954);
#12069=ADVANCED_FACE('',(#1560),#993,.F.);
#12070=ADVANCED_FACE('',(#1561),#994,.F.);
#12071=ADVANCED_FACE('',(#1562),#995,.F.);
#12072=ADVANCED_FACE('',(#1563),#996,.F.);
#12073=ADVANCED_FACE('',(#1564),#997,.F.);
#12074=ADVANCED_FACE('',(#1565),#998,.F.);
#12075=ADVANCED_FACE('',(#1566),#999,.F.);
#12076=ADVANCED_FACE('',(#1567),#1000,.F.);
#12077=ADVANCED_FACE('',(#1568),#1001,.F.);
#12078=ADVANCED_FACE('',(#1569),#1002,.T.);
#12079=ADVANCED_FACE('',(#1570),#485,.T.);
#12080=ADVANCED_FACE('',(#1571),#11741,.T.);
#12081=ADVANCED_FACE('',(#1572),#486,.T.);
#12082=ADVANCED_FACE('',(#1573,#811),#1003,.T.);
#12083=ADVANCED_FACE('',(#1574),#487,.T.);
#12084=ADVANCED_FACE('',(#1575),#11742,.T.);
#12512=CLOSED_SHELL('',(#12069,#12070,#12071,#12072,#12073,#12074,#12075,
#12076));
#12513=CLOSED_SHELL('',(#12077,#12078,#12079,#12080,#12081,#12082,#12083,
#12084));
#13542=AXIS2_PLACEMENT_3D('',#19248,#15588,#15589);
#13543=AXIS2_PLACEMENT_3D('',#19249,#15590,#15591);
#13544=AXIS2_PLACEMENT_3D('',#19258,#15596,#15597);
#13545=AXIS2_PLACEMENT_3D('',#19264,#15601,#15602);
#13546=AXIS2_PLACEMENT_3D('',#19270,#15606,#15607);
#13547=AXIS2_PLACEMENT_3D('',#19276,#15611,#15612);
#13548=AXIS2_PLACEMENT_3D('',#19282,#15616,#15617);
#13549=AXIS2_PLACEMENT_3D('',#19285,#15620,#15621);
#13550=AXIS2_PLACEMENT_3D('',#19286,#15622,#15623);
#13551=AXIS2_PLACEMENT_3D('',#19287,#15624,#15625);
#13552=AXIS2_PLACEMENT_3D('',#19289,#15626,#15627);
#13553=AXIS2_PLACEMENT_3D('',#19290,#15628,#15629);
#13554=AXIS2_PLACEMENT_3D('',#19292,#15630,#15631);
#13555=AXIS2_PLACEMENT_3D('',#19293,#15632,#15633);
#13556=AXIS2_PLACEMENT_3D('',#19295,#15634,#15635);
#13557=AXIS2_PLACEMENT_3D('',#19297,#15637,#15638);
#13558=AXIS2_PLACEMENT_3D('',#19299,#15639,#15640);
#13559=AXIS2_PLACEMENT_3D('',#19301,#15642,#15643);
#13560=AXIS2_PLACEMENT_3D('',#19303,#15644,#15645);
#13561=AXIS2_PLACEMENT_3D('',#19305,#15647,#15648);
#13562=AXIS2_PLACEMENT_3D('',#19307,#15649,#15650);
#13563=AXIS2_PLACEMENT_3D('',#19308,#15651,#15652);
#13564=AXIS2_PLACEMENT_3D('',#19310,#15653,#15654);
#13565=AXIS2_PLACEMENT_3D('',#19312,#15656,#15657);
#15588=DIRECTION('axis',(0.,0.,1.));
#15589=DIRECTION('refdir',(1.,0.,0.));
#15590=DIRECTION('center_axis',(0.866025403784439,0.,-0.5));
#15591=DIRECTION('ref_axis',(0.5,0.,0.866025403784439));
#15592=DIRECTION('',(-0.5,0.,-0.866025403784439));
#15593=DIRECTION('',(0.,-1.,0.));
#15594=DIRECTION('',(0.5,0.,0.866025403784439));
#15595=DIRECTION('',(0.,-1.,0.));
#15596=DIRECTION('center_axis',(1.60246890531964E-16,0.,-1.));
#15597=DIRECTION('ref_axis',(1.,0.,1.60246890531964E-16));
#15598=DIRECTION('',(-1.,0.,-1.60246890531964E-16));
#15599=DIRECTION('',(0.,-1.,0.));
#15600=DIRECTION('',(1.,0.,1.60246890531964E-16));
#15601=DIRECTION('center_axis',(-0.866025403784439,0.,-0.5));
#15602=DIRECTION('ref_axis',(0.5,0.,-0.866025403784439));
#15603=DIRECTION('',(-0.5,0.,0.866025403784439));
#15604=DIRECTION('',(0.,-1.,0.));
#15605=DIRECTION('',(0.5,0.,-0.866025403784439));
#15606=DIRECTION('center_axis',(-0.866025403784439,0.,0.5));
#15607=DIRECTION('ref_axis',(-0.5,0.,-0.866025403784439));
#15608=DIRECTION('',(0.5,0.,0.866025403784439));
#15609=DIRECTION('',(0.,-1.,0.));
#15610=DIRECTION('',(-0.5,0.,-0.866025403784439));
#15611=DIRECTION('center_axis',(-1.60246890531964E-16,0.,1.));
#15612=DIRECTION('ref_axis',(-1.,0.,-1.60246890531964E-16));
#15613=DIRECTION('',(1.,0.,1.60246890531964E-16));
#15614=DIRECTION('',(0.,-1.,0.));
#15615=DIRECTION('',(-1.,0.,-1.60246890531964E-16));
#15616=DIRECTION('center_axis',(0.866025403784439,0.,0.5));
#15617=DIRECTION('ref_axis',(-0.5,0.,0.866025403784439));
#15618=DIRECTION('',(0.5,0.,-0.866025403784439));
#15619=DIRECTION('',(-0.5,0.,0.866025403784439));
#15620=DIRECTION('center_axis',(0.,1.,0.));
#15621=DIRECTION('ref_axis',(1.,0.,0.));
#15622=DIRECTION('center_axis',(0.,-1.,0.));
#15623=DIRECTION('ref_axis',(0.,0.,-1.));
#15624=DIRECTION('center_axis',(0.,1.,0.));
#15625=DIRECTION('ref_axis',(1.,0.,0.));
#15626=DIRECTION('center_axis',(0.,1.,0.));
#15627=DIRECTION('ref_axis',(1.,0.,0.));
#15628=DIRECTION('center_axis',(0.,1.,0.));
#15629=DIRECTION('ref_axis',(0.,0.,1.));
#15630=DIRECTION('center_axis',(0.,-1.,0.));
#15631=DIRECTION('ref_axis',(1.,0.,0.));
#15632=DIRECTION('center_axis',(0.,-1.,0.));
#15633=DIRECTION('ref_axis',(1.,0.,0.));
#15634=DIRECTION('center_axis',(0.,-1.,0.));
#15635=DIRECTION('ref_axis',(1.,0.,0.));
#15636=DIRECTION('',(0.707106781186547,0.707106781186548,8.65956056235493E-17));
#15637=DIRECTION('center_axis',(0.,-1.,0.));
#15638=DIRECTION('ref_axis',(1.,0.,0.));
#15639=DIRECTION('center_axis',(0.,-1.,0.));
#15640=DIRECTION('ref_axis',(1.,0.,0.));
#15641=DIRECTION('',(0.,1.,0.));
#15642=DIRECTION('center_axis',(0.,1.,0.));
#15643=DIRECTION('ref_axis',(1.,0.,0.));
#15644=DIRECTION('center_axis',(0.,-1.,0.));
#15645=DIRECTION('ref_axis',(1.,0.,0.));
#15646=DIRECTION('',(-0.707106781186547,0.707106781186548,-8.65956056235493E-17));
#15647=DIRECTION('center_axis',(0.,-1.,0.));
#15648=DIRECTION('ref_axis',(0.,0.,-1.));
#15649=DIRECTION('center_axis',(0.,-1.,0.));
#15650=DIRECTION('ref_axis',(1.,0.,0.));
#15651=DIRECTION('center_axis',(0.,1.,0.));
#15652=DIRECTION('ref_axis',(1.,0.,0.));
#15653=DIRECTION('center_axis',(0.,1.,0.));
#15654=DIRECTION('ref_axis',(1.,0.,0.));
#15655=DIRECTION('',(-0.447213595499958,0.894427190999916,-5.47678698264203E-17));
#15656=DIRECTION('center_axis',(0.,-1.,0.));
#15657=DIRECTION('ref_axis',(1.,0.,0.));
#15658=DIRECTION('',(0.,1.,0.));
#19248=CARTESIAN_POINT('',(0.,0.,0.));
#19249=CARTESIAN_POINT('Origin',(0.0866025403784439,-0.4,-0.15));
#19250=CARTESIAN_POINT('',(0.173205080756888,-0.4,0.));
#19251=CARTESIAN_POINT('',(0.0866025403784439,-0.4,-0.15));
#19252=CARTESIAN_POINT('',(0.173205080756888,-0.4,0.));
#19253=CARTESIAN_POINT('',(0.0866025403784439,-0.64,-0.15));
#19254=CARTESIAN_POINT('',(0.0866025403784439,-0.4,-0.15));
#19255=CARTESIAN_POINT('',(0.173205080756888,-0.64,0.));
#19256=CARTESIAN_POINT('',(0.173205080756888,-0.64,0.));
#19257=CARTESIAN_POINT('',(0.173205080756888,-0.4,0.));
#19258=CARTESIAN_POINT('Origin',(-0.0866025403784438,-0.4,-0.15));
#19259=CARTESIAN_POINT('',(-0.0866025403784438,-0.4,-0.15));
#19260=CARTESIAN_POINT('',(0.0866025403784439,-0.4,-0.15));
#19261=CARTESIAN_POINT('',(-0.0866025403784438,-0.64,-0.15));
#19262=CARTESIAN_POINT('',(-0.0866025403784438,-0.4,-0.15));
#19263=CARTESIAN_POINT('',(0.0866025403784439,-0.64,-0.15));
#19264=CARTESIAN_POINT('Origin',(-0.173205080756888,-0.4,-2.77555756156289E-17));
#19265=CARTESIAN_POINT('',(-0.173205080756888,-0.4,-2.12115047744981E-17));
#19266=CARTESIAN_POINT('',(-0.0866025403784438,-0.4,-0.15));
#19267=CARTESIAN_POINT('',(-0.173205080756888,-0.64,-2.77555756156289E-17));
#19268=CARTESIAN_POINT('',(-0.173205080756888,-0.4,-2.12115047744981E-17));
#19269=CARTESIAN_POINT('',(-0.0866025403784438,-0.64,-0.15));
#19270=CARTESIAN_POINT('Origin',(-0.0866025403784439,-0.4,0.15));
#19271=CARTESIAN_POINT('',(-0.0866025403784439,-0.4,0.15));
#19272=CARTESIAN_POINT('',(-0.173205080756888,-0.4,-2.12115047744981E-17));
#19273=CARTESIAN_POINT('',(-0.0866025403784439,-0.64,0.15));
#19274=CARTESIAN_POINT('',(-0.0866025403784439,-0.4,0.15));
#19275=CARTESIAN_POINT('',(-0.173205080756888,-0.64,-2.12115047744981E-17));
#19276=CARTESIAN_POINT('Origin',(0.0866025403784439,-0.4,0.15));
#19277=CARTESIAN_POINT('',(0.0866025403784439,-0.4,0.15));
#19278=CARTESIAN_POINT('',(-0.0866025403784439,-0.4,0.15));
#19279=CARTESIAN_POINT('',(0.0866025403784439,-0.64,0.15));
#19280=CARTESIAN_POINT('',(0.0866025403784439,-0.4,0.15));
#19281=CARTESIAN_POINT('',(-0.0866025403784439,-0.64,0.15));
#19282=CARTESIAN_POINT('Origin',(0.173205080756888,-0.4,0.));
#19283=CARTESIAN_POINT('',(0.0866025403784439,-0.4,0.15));
#19284=CARTESIAN_POINT('',(0.0866025403784439,-0.64,0.15));
#19285=CARTESIAN_POINT('Origin',(0.,-0.4,-2.77555756156289E-17));
#19286=CARTESIAN_POINT('Origin',(0.,-0.64,-2.77555756156289E-17));
#19287=CARTESIAN_POINT('Origin',(0.,-1.,0.));
#19288=CARTESIAN_POINT('',(-0.1954,-1.,2.39295984553393E-17));
#19289=CARTESIAN_POINT('Origin',(0.,-1.,0.));
#19290=CARTESIAN_POINT('Origin',(0.3,0.4,0.));
#19291=CARTESIAN_POINT('',(-0.3,0.4,-3.67394039744206E-17));
#19292=CARTESIAN_POINT('Origin',(0.,0.4,0.));
#19293=CARTESIAN_POINT('Origin',(0.,0.375,0.));
#19294=CARTESIAN_POINT('',(-0.35,0.35,-4.28626379701573E-17));
#19295=CARTESIAN_POINT('Origin',(0.,0.35,0.));
#19296=CARTESIAN_POINT('',(-0.325,0.375,-3.9801020972289E-17));
#19297=CARTESIAN_POINT('Origin',(0.,0.19,0.));
#19298=CARTESIAN_POINT('',(-0.35,0.03,-4.28626379701574E-17));
#19299=CARTESIAN_POINT('Origin',(0.,0.03,0.));
#19300=CARTESIAN_POINT('',(-0.35,0.19,-4.28626379701574E-17));
#19301=CARTESIAN_POINT('Origin',(0.,0.0149999999999999,0.));
#19302=CARTESIAN_POINT('',(-0.32,-3.29597460435593E-17,-3.91886975727153E-17));
#19303=CARTESIAN_POINT('Origin',(0.,0.,0.));
#19304=CARTESIAN_POINT('',(-0.335,0.0149999999999999,-4.10256677714363E-17));
#19305=CARTESIAN_POINT('Origin',(0.22,0.,0.));
#19306=CARTESIAN_POINT('',(-0.22,-6.93889390390723E-18,-2.69422295812418E-17));
#19307=CARTESIAN_POINT('Origin',(0.,0.,0.));
#19308=CARTESIAN_POINT('Origin',(0.,-0.02,0.));
#19309=CARTESIAN_POINT('',(-0.1954,-0.0492,2.39295984553393E-17));
#19310=CARTESIAN_POINT('Origin',(0.,-0.0492,0.));
#19311=CARTESIAN_POINT('',(-0.21,-0.02,-2.57175827820944E-17));
#19312=CARTESIAN_POINT('Origin',(0.,-0.8,0.));
#19313=CARTESIAN_POINT('',(-0.1954,-0.8,-2.39295984553393E-17));
#32678=UNCERTAINTY_MEASURE_WITH_UNIT(LENGTH_MEASURE(0.001),#32752,
'DISTANCE_ACCURACY_VALUE',
'Maximum model space distance between geometric entities at asserted c
onnectivities');
#32702=UNCERTAINTY_MEASURE_WITH_UNIT(LENGTH_MEASURE(0.001),#32752,
'DISTANCE_ACCURACY_VALUE',
'Maximum model space distance between geometric entities at asserted c
onnectivities');
#32727=(
GEOMETRIC_REPRESENTATION_CONTEXT(3)
GLOBAL_UNCERTAINTY_ASSIGNED_CONTEXT((#32678))
GLOBAL_UNIT_ASSIGNED_CONTEXT((#32752,#32754,#32755))
REPRESENTATION_CONTEXT('','3D')
);
#32751=(
GEOMETRIC_REPRESENTATION_CONTEXT(3)
GLOBAL_UNCERTAINTY_ASSIGNED_CONTEXT((#32702))
GLOBAL_UNIT_ASSIGNED_CONTEXT((#32752,#32754,#32755))
REPRESENTATION_CONTEXT('','3D')
);
#32752=(
LENGTH_UNIT()
NAMED_UNIT(*)
SI_UNIT(.CENTI.,.METRE.)
);
#32754=(
NAMED_UNIT(*)
PLANE_ANGLE_UNIT()
SI_UNIT($,.RADIAN.)
);
#32755=(
NAMED_UNIT(*)
SI_UNIT($,.STERADIAN.)
SOLID_ANGLE_UNIT()
);
#32780=SHAPE_DEFINITION_REPRESENTATION(#32833,#32953);
#32833=PRODUCT_DEFINITION_SHAPE('',$,#33002);
#32953=SHAPE_REPRESENTATION('',(#13542),#32727);
#32977=PRODUCT_DEFINITION_CONTEXT('part definition',#33123,'design');
#33002=PRODUCT_DEFINITION('M4x10 Cap Screw','M4x10 Cap Screw',#33050,#32977);
#33050=PRODUCT_DEFINITION_FORMATION('',$,#33149);
#33123=APPLICATION_CONTEXT(
'Core Data for Automotive Mechanical Design Process');
#33124=PRODUCT_CONTEXT('part definition',#33123,'mechanical');
#33149=PRODUCT('M4x10 Cap Screw','M4x10 Cap Screw','M4x10 Cap Screw',(#33124));
#33243=COLOUR_RGB('Black',0.12,0.14,0.17);
#33244=FILL_AREA_STYLE_COLOUR('',#33243);
#33245=FILL_AREA_STYLE('',(#33244));
#33246=SURFACE_STYLE_FILL_AREA(#33245);
#33247=SURFACE_SIDE_STYLE('',(#33246));
#33248=SURFACE_STYLE_USAGE(.BOTH.,#33247);
#33249=PRESENTATION_STYLE_ASSIGNMENT((#33248));
ENDSEC;
END-ISO-10303-21;
